ISO-10303-21;
HEADER;
FILE_DESCRIPTION (('STEP AP214'),
    '1' );
FILE_NAME ('socket head cap screw_iso_ISO 4762 M5 x 16 - 16N.step',
    '2026-10-24T07:08:27',
    ( '' ),
    ( '' ),
    'SwSTEP 2.0',
    'SolidWorks 2026',
    '' );
FILE_SCHEMA (( 'AUTOMOTIVE_DESIGN' ));
ENDSEC;

DATA;
#30=VECTOR ( 'NONE', #9447, 1000.000000000000000 ) ;
#89=DIRECTION ( 'NONE',  ( 1.000000000000000000, 0.000000000000000000, 0.000000000000000000 ) ) ;
#94=PLANE ( 'NONE',  #12371 ) ;
#108=ORIENTED_EDGE ( 'NONE', *, *, #12094, .T. ) ;
#122=DIRECTION ( 'NONE',  ( 0.000000000000000000, 0.000000000000000000, 1.000000000000000000 ) ) ;
#158=ORIENTED_EDGE ( 'NONE', *, *, #15306, .F. ) ;
#159=FACE_OUTER_BOUND ( 'NONE', #7289, .T. ) ;
#160=AXIS2_PLACEMENT_3D ( 'NONE', #16421, #7559, #15796 ) ;
#177=EDGE_CURVE ( 'NONE', #2698, #7707, #13480, .T. ) ;
#180=VECTOR ( 'NONE', #16052, 1000.000000000000000 ) ;
#183=DIRECTION ( 'NONE',  ( -0.000000000000000000, 1.000000000000000000, 1.224646799147353207E-16 ) ) ;
#193=LINE ( 'NONE', #5991, #9405 ) ;
#232=DIRECTION ( 'NONE',  ( -1.000000000000000000, -0.000000000000000000, -0.000000000000000000 ) ) ;
#254=UNCERTAINTY_MEASURE_WITH_UNIT (LENGTH_MEASURE( 1.000000000000000082E-05 ), #934, 'distance_accuracy_value', 'NONE');
#278=DIRECTION ( 'NONE',  ( 1.000000000000000000, 0.000000000000000000, 0.000000000000000000 ) ) ;
#335=EDGE_LOOP ( 'NONE', ( #6320, #13765, #5503, #3259, #11558 ) ) ;
#349=CARTESIAN_POINT ( 'NONE',  ( 5.200000000000002842, 0.000000000000000000, 2.500000000000000444 ) ) ;
#473=CIRCLE ( 'NONE', #160, 4.000000000000000000 ) ;
#476=EDGE_CURVE ( 'NONE', #7314, #5247, #9708, .T. ) ;
#479=TOROIDAL_SURFACE ( 'NONE', #9907, 4.000000000000000000, 0.2500000000000000000 ) ;
#529=AXIS2_PLACEMENT_3D ( 'NONE', #16197, #4487, #18349 ) ;
#531=EDGE_CURVE ( 'NONE', #4599, #15674, #9181, .T. ) ;
#554=ORIENTED_EDGE ( 'NONE', *, *, #177, .T. ) ;
#570=DIRECTION ( 'NONE',  ( 1.000000000000000000, 0.000000000000000000, 0.000000000000000000 ) ) ;
#602=AXIS2_PLACEMENT_3D ( 'NONE', #15281, #16437, #16812 ) ;
#612=DIRECTION ( 'NONE',  ( -0.7071067811865364705, 8.659560562355067211E-17, -0.7071067811865584529 ) ) ;
#666=CARTESIAN_POINT ( 'NONE',  ( 5.200000000000002842, 0.000000000000000000, 0.000000000000000000 ) ) ;
#752=VERTEX_POINT ( 'NONE', #4902 ) ;
#762=DIRECTION ( 'NONE',  ( -1.000000000000000000, -0.000000000000000000, -0.000000000000000000 ) ) ;
#804=PLANE ( 'NONE',  #2228 ) ;
#811=DIRECTION ( 'NONE',  ( 0.000000000000000000, 1.000000000000000000, -1.224646799147353207E-16 ) ) ;
#862=CARTESIAN_POINT ( 'NONE',  ( -31.74999999999995737, 0.000000000000000000, 0.000000000000000000 ) ) ;
#916=ORIENTED_EDGE ( 'NONE', *, *, #16337, .F. ) ;
#924=CARTESIAN_POINT ( 'NONE',  ( 2.500000000000000000, -2.357898499370432166, 3.035766082959412415E-15 ) ) ;
#933=AXIS2_PLACEMENT_3D ( 'NONE', #17379, #1641, #13097 ) ;
#934=( LENGTH_UNIT ( ) NAMED_UNIT ( * ) SI_UNIT ( .MILLI., .METRE. ) );
#939=LINE ( 'NONE', #5113, #18715 ) ;
#966=EDGE_CURVE ( 'NONE', #7707, #2762, #16570, .T. ) ;
#969=CARTESIAN_POINT ( 'NONE',  ( 2.500000000000000000, 0.000000000000000000, 0.000000000000000000 ) ) ;
#1012=DIRECTION ( 'NONE',  ( 0.000000000000000000, 0.4999999999999990008, -0.8660254037844391517 ) ) ;
#1021=SHAPE_REPRESENTATION_RELATIONSHIP ( 'NONE' , 'NONE' ,  #8256, #4884 ) ;
#1023=DIRECTION ( 'NONE',  ( 0.000000000000000000, 0.000000000000000000, 1.000000000000000000 ) ) ;
#1035=CARTESIAN_POINT ( 'NONE',  ( 2.500000000000000000, -1.178949249685214307, 2.042000000000001592 ) ) ;
#1056=CARTESIAN_POINT ( 'NONE',  ( 2.500000000000000000, 0.000000000000000000, 0.000000000000000000 ) ) ;
#1059=DIRECTION ( 'NONE',  ( 1.000000000000000000, 0.000000000000000000, 0.000000000000000000 ) ) ;
#1103=CARTESIAN_POINT ( 'NONE',  ( 2.500000000000000000, -2.357898499370432166, 3.035766082959412415E-15 ) ) ;
#1122=AXIS2_PLACEMENT_3D ( 'NONE', #9107, #3209, #11872 ) ;
#1124=DIRECTION ( 'NONE',  ( -1.000000000000000000, -0.000000000000000000, -0.000000000000000000 ) ) ;
#1206=ADVANCED_FACE ( 'NONE', ( #12866 ), #2856, .F. ) ;
#1224=ORIENTED_EDGE ( 'NONE', *, *, #8262, .F. ) ;
#1279=VERTEX_POINT ( 'NONE', #3788 ) ;
#1282=ORIENTED_EDGE ( 'NONE', *, *, #14553, .T. ) ;
#1298=CARTESIAN_POINT ( 'NONE',  ( -31.74999999999995737, 0.000000000000000000, 4.250000000000000000 ) ) ;
#1329=DIRECTION ( 'NONE',  ( 0.000000000000000000, 0.000000000000000000, -1.000000000000000000 ) ) ;
#1344=FACE_OUTER_BOUND ( 'NONE', #5692, .T. ) ;
#1348=CARTESIAN_POINT ( 'NONE',  ( 2.500000000000000000, -1.178949249685214307, 2.042000000000001592 ) ) ;
#1362=DIRECTION ( 'NONE',  ( 1.000000000000000000, 0.000000000000000000, 0.000000000000000000 ) ) ;
#1410=ORIENTED_EDGE ( 'NONE', *, *, #531, .T. ) ;
#1479=ORIENTED_EDGE ( 'NONE', *, *, #10684, .F. ) ;
#1509=CIRCLE ( 'NONE', #14580, 2.041999999999999815 ) ;
#1530=DIRECTION ( 'NONE',  ( 1.000000000000000000, 0.000000000000000000, 0.000000000000000000 ) ) ;
#1541=FACE_OUTER_BOUND ( 'NONE', #10983, .T. ) ;
#1587=ORIENTED_EDGE ( 'NONE', *, *, #7596, .F. ) ;
#1626=VERTEX_POINT ( 'NONE', #18597 ) ;
#1641=DIRECTION ( 'NONE',  ( 0.000000000000000000, 0.8660254037844380415, -0.5000000000000012212 ) ) ;
#1668=CARTESIAN_POINT ( 'NONE',  ( 2.500000000000000000, 1.178949249685212974, -2.042000000000001148 ) ) ;
#1671=CIRCLE ( 'NONE', #10918, 2.500000000000000444 ) ;
#1708=APPLICATION_CONTEXT ( 'automotive_design' ) ;
#1726=AXIS2_PLACEMENT_3D ( 'NONE', #18666, #5615, #11422 ) ;
#1752=AXIS2_PLACEMENT_3D ( 'NONE', #17869, #13494, #7758 ) ;
#1755=CARTESIAN_POINT ( 'NONE',  ( 2.500000000000000000, 1.178949249685217415, 2.041999999999998483 ) ) ;
#1788=VECTOR ( 'NONE', #11330, 1000.000000000000114 ) ;
#1934=ORIENTED_EDGE ( 'NONE', *, *, #16162, .T. ) ;
#1972=ORIENTED_EDGE ( 'NONE', *, *, #9121, .T. ) ;
#1974=CARTESIAN_POINT ( 'NONE',  ( 20.55500000000001748, 0.000000000000000000, 0.000000000000000000 ) ) ;
#1987=CYLINDRICAL_SURFACE ( 'NONE', #13662, 4.250000000000000000 ) ;
#2059=VERTEX_POINT ( 'NONE', #7710 ) ;
#2098=CIRCLE ( 'NONE', #12144, 2.041999999999999815 ) ;
#2143=EDGE_CURVE ( 'NONE', #17667, #6907, #18287, .T. ) ;
#2166=EDGE_CURVE ( 'NONE', #2762, #3664, #12104, .T. ) ;
#2201=ORIENTED_EDGE ( 'NONE', *, *, #2863, .T. ) ;
#2207=ORIENTED_EDGE ( 'NONE', *, *, #17907, .F. ) ;
#2211=FACE_OUTER_BOUND ( 'NONE', #8833, .T. ) ;
#2228=AXIS2_PLACEMENT_3D ( 'NONE', #5076, #11170, #17000 ) ;
#2319=CARTESIAN_POINT ( 'NONE',  ( 2.500000000000000000, 1.768423874527822459, -1.021000000000002794 ) ) ;
#2353=CIRCLE ( 'NONE', #18786, 2.041999999999999815 ) ;
#2362=EDGE_CURVE ( 'NONE', #18341, #1279, #6951, .T. ) ;
#2420=CARTESIAN_POINT ( 'NONE',  ( 2.500000000000000000, 2.357898499370431722, -2.818925648462311528E-15 ) ) ;
#2445=CARTESIAN_POINT ( 'NONE',  ( 2.500000000000000000, 0.000000000000000000, 0.000000000000000000 ) ) ;
#2456=FACE_OUTER_BOUND ( 'NONE', #335, .T. ) ;
#2495=AXIS2_PLACEMENT_3D ( 'NONE', #8563, #89, #1329 ) ;
#2563=LINE ( 'NONE', #18758, #1788 ) ;
#2579=EDGE_CURVE ( 'NONE', #1626, #4084, #16656, .T. ) ;
#2610=EDGE_CURVE ( 'NONE', #5270, #3414, #9698, .T. ) ;
#2611=FACE_OUTER_BOUND ( 'NONE', #13479, .T. ) ;
#2627=( NAMED_UNIT ( * ) PLANE_ANGLE_UNIT ( ) SI_UNIT ( $, .RADIAN. ) );
#2635=CARTESIAN_POINT ( 'NONE',  ( 2.500000000000000000, 0.000000000000000000, 0.000000000000000000 ) ) ;
#2649=PLANE ( 'NONE',  #7273 ) ;
#2698=VERTEX_POINT ( 'NONE', #3897 ) ;
#2744=CARTESIAN_POINT ( 'NONE',  ( 21.00000000000000000, 2.055000000000000160, 0.000000000000000000 ) ) ;
#2753=ADVANCED_FACE ( 'NONE', ( #17223 ), #2649, .T. ) ;
#2762=VERTEX_POINT ( 'NONE', #10163 ) ;
#2777=DIRECTION ( 'NONE',  ( 0.000000000000000000, 0.000000000000000000, 1.000000000000000000 ) ) ;
#2790=EDGE_LOOP ( 'NONE', ( #1972, #4474, #11804 ) ) ;
#2824=FACE_OUTER_BOUND ( 'NONE', #16537, .T. ) ;
#2830=DIRECTION ( 'NONE',  ( 1.000000000000000000, 0.000000000000000000, 0.000000000000000000 ) ) ;
#2856=PLANE ( 'NONE',  #11771 ) ;
#2863=EDGE_CURVE ( 'NONE', #16191, #5775, #6889, .T. ) ;
#2921=ORIENTED_EDGE ( 'NONE', *, *, #2579, .F. ) ;
#2940=CARTESIAN_POINT ( 'NONE',  ( 0.000000000000000000, 0.000000000000000000, 0.000000000000000000 ) ) ;
#2949=VECTOR ( 'NONE', #11136, 1000.000000000000000 ) ;
#2972=ORIENTED_EDGE ( 'NONE', *, *, #2579, .T. ) ;
#2973=DIRECTION ( 'NONE',  ( -1.000000000000000000, -0.000000000000000000, -0.000000000000000000 ) ) ;
#2975=AXIS2_PLACEMENT_3D ( 'NONE', #2744, #5690, #3026 ) ;
#2978=DIRECTION ( 'NONE',  ( -1.000000000000000000, -0.000000000000000000, -0.000000000000000000 ) ) ;
#2984=FACE_OUTER_BOUND ( 'NONE', #8511, .T. ) ;
#3003=CARTESIAN_POINT ( 'NONE',  ( 0.000000000000000000, -1.178949249685214307, 2.042000000000001592 ) ) ;
#3005=EDGE_LOOP ( 'NONE', ( #108, #11824 ) ) ;
#3026=DIRECTION ( 'NONE',  ( 0.000000000000000000, 0.000000000000000000, -1.000000000000000000 ) ) ;
#3118=ORIENTED_EDGE ( 'NONE', *, *, #2143, .F. ) ;
#3128=ORIENTED_EDGE ( 'NONE', *, *, #9130, .T. ) ;
#3196=EDGE_CURVE ( 'NONE', #6730, #16191, #18534, .T. ) ;
#3209=DIRECTION ( 'NONE',  ( 1.000000000000000000, 0.000000000000000000, 0.000000000000000000 ) ) ;
#3238=PLANE ( 'NONE',  #17315 ) ;
#3259=ORIENTED_EDGE ( 'NONE', *, *, #15306, .T. ) ;
#3278=DIRECTION ( 'NONE',  ( -1.000000000000000000, -0.000000000000000000, -0.000000000000000000 ) ) ;
#3374=FACE_OUTER_BOUND ( 'NONE', #8792, .T. ) ;
#3395=ORIENTED_EDGE ( 'NONE', *, *, #5622, .T. ) ;
#3414=VERTEX_POINT ( 'NONE', #14013 ) ;
#3473=ORIENTED_EDGE ( 'NONE', *, *, #17289, .F. ) ;
#3510=CARTESIAN_POINT ( 'NONE',  ( 2.500000000000000000, 2.357898499370431722, -2.818925648462311528E-15 ) ) ;
#3577=ORIENTED_EDGE ( 'NONE', *, *, #10569, .T. ) ;
#3663=FACE_OUTER_BOUND ( 'NONE', #2790, .T. ) ;
#3664=VERTEX_POINT ( 'NONE', #15040 ) ;
#3715=AXIS2_PLACEMENT_3D ( 'NONE', #2940, #17238, #4370 ) ;
#3750=ORIENTED_EDGE ( 'NONE', *, *, #9344, .T. ) ;
#3788=CARTESIAN_POINT ( 'NONE',  ( 5.000000000000002665, 0.000000000000000000, -2.700000000000000622 ) ) ;
#3805=MANIFOLD_SOLID_BREP ( 'Hex', #18036 ) ;
#3825=ORIENTED_EDGE ( 'NONE', *, *, #9715, .F. ) ;
#3844=PLANE ( 'NONE',  #10575 ) ;
#3897=CARTESIAN_POINT ( 'NONE',  ( 4.999999999999997335, 0.000000000000000000, 4.250000000000000000 ) ) ;
#3903=ORIENTED_EDGE ( 'NONE', *, *, #7498, .F. ) ;
#3911=VECTOR ( 'NONE', #5236, 1000.000000000000000 ) ;
#3915=ORIENTED_EDGE ( 'NONE', *, *, #5033, .T. ) ;
#3916=FACE_BOUND ( 'NONE', #16355, .T. ) ;
#3921=DIRECTION ( 'NONE',  ( 1.000000000000000000, 0.000000000000000000, 0.000000000000000000 ) ) ;
#3974=VECTOR ( 'NONE', #14333, 1000.000000000000000 ) ;
#4011=VECTOR ( 'NONE', #5766, 1000.000000000000114 ) ;
#4014=DIRECTION ( 'NONE',  ( -1.000000000000000000, -0.000000000000000000, -0.000000000000000000 ) ) ;
#4040=EDGE_LOOP ( 'NONE', ( #5014, #3118, #16213, #8341, #14044 ) ) ;
#4043=PRODUCT ( 'socket head cap screw_iso_ISO 4762 M5 x 16 - 16N', 'socket head cap screw_iso_ISO 4762 M5 x 16 - 16N', '', ( #17185 ) ) ;
#4064=ORIENTED_EDGE ( 'NONE', *, *, #966, .T. ) ;
#4084=VERTEX_POINT ( 'NONE', #7765 ) ;
#4092=CARTESIAN_POINT ( 'NONE',  ( 2.500000000000000000, -1.178949249685218748, -2.041999999999998039 ) ) ;
#4161=CARTESIAN_POINT ( 'NONE',  ( 2.500000000000000000, -1.178949249685214307, 2.042000000000001592 ) ) ;
#4168=DIRECTION ( 'NONE',  ( 0.000000000000000000, 1.000000000000000000, -1.287488025362403787E-15 ) ) ;
#4184=EDGE_LOOP ( 'NONE', ( #18752, #7134, #1587, #7545 ) ) ;
#4253=ORIENTED_EDGE ( 'NONE', *, *, #5918, .T. ) ;
#4259=ORIENTED_EDGE ( 'NONE', *, *, #531, .F. ) ;
#4281=ORIENTED_EDGE ( 'NONE', *, *, #12573, .F. ) ;
#4318=CARTESIAN_POINT ( 'NONE',  ( 4.999999999999997335, 0.000000000000000000, 0.000000000000000000 ) ) ;
#4338=ORIENTED_EDGE ( 'NONE', *, *, #2610, .F. ) ;
#4357=EDGE_CURVE ( 'NONE', #15093, #10166, #10238, .T. ) ;
#4370=DIRECTION ( 'NONE',  ( 0.000000000000000000, 0.000000000000000000, 1.000000000000000000 ) ) ;
#4391=CARTESIAN_POINT ( 'NONE',  ( 2.500000000000000000, 2.357898499370431722, -2.818925648462311528E-15 ) ) ;
#4444=VECTOR ( 'NONE', #8898, 1000.000000000000000 ) ;
#4474=ORIENTED_EDGE ( 'NONE', *, *, #14602, .F. ) ;
#4487=DIRECTION ( 'NONE',  ( -1.000000000000000000, -0.000000000000000000, -0.000000000000000000 ) ) ;
#4492=EDGE_CURVE ( 'NONE', #752, #6265, #16148, .T. ) ;
#4527=VECTOR ( 'NONE', #5420, 1000.000000000000000 ) ;
#4529=CARTESIAN_POINT ( 'NONE',  ( 2.500000000000000000, 2.357898499370431722, -2.818925648462311528E-15 ) ) ;
#4539=ORIENTED_EDGE ( 'NONE', *, *, #8599, .T. ) ;
#4555=EDGE_LOOP ( 'NONE', ( #11172, #10972, #14571, #7323 ) ) ;
#4575=EDGE_CURVE ( 'NONE', #5775, #18341, #9926, .T. ) ;
#4599=VERTEX_POINT ( 'NONE', #2319 ) ;
#4647=FACE_OUTER_BOUND ( 'NONE', #16602, .T. ) ;
#4680=EDGE_LOOP ( 'NONE', ( #12179, #18446, #11092 ) ) ;
#4854=DIRECTION ( 'NONE',  ( 0.000000000000000000, 0.000000000000000000, -1.000000000000000000 ) ) ;
#4857=ADVANCED_FACE ( 'NONE', ( #3916, #15528 ), #94, .T. ) ;
#4883=CARTESIAN_POINT ( 'NONE',  ( -31.74999999999995737, 0.000000000000000000, 2.500000000000000444 ) ) ;
#4884=ADVANCED_BREP_SHAPE_REPRESENTATION ( '', ( #3805, #8017 ), #7430 ) ;
#4902=CARTESIAN_POINT ( 'NONE',  ( 2.500000000000000000, 1.178949249685217415, 2.041999999999998483 ) ) ;
#4979=DIRECTION ( 'NONE',  ( -1.000000000000000000, -0.000000000000000000, -0.000000000000000000 ) ) ;
#4996=ORIENTED_EDGE ( 'NONE', *, *, #16337, .T. ) ;
#5014=ORIENTED_EDGE ( 'NONE', *, *, #12252, .F. ) ;
#5017=CARTESIAN_POINT ( 'NONE',  ( 2.500000000000000000, 1.178949249685212974, -2.042000000000001148 ) ) ;
#5033=EDGE_CURVE ( 'NONE', #6730, #13493, #14204, .T. ) ;
#5071=LINE ( 'NONE', #7929, #15978 ) ;
#5076=CARTESIAN_POINT ( 'NONE',  ( 2.500000000000000000, -2.357898499370432166, 3.035766082959412415E-15 ) ) ;
#5091=DIRECTION ( 'NONE',  ( 0.000000000000000000, 0.000000000000000000, 1.000000000000000000 ) ) ;
#5113=CARTESIAN_POINT ( 'NONE',  ( 0.000000000000000000, -2.357898499370432166, 3.035766082959412415E-15 ) ) ;
#5236=DIRECTION ( 'NONE',  ( -1.000000000000000000, -0.000000000000000000, -0.000000000000000000 ) ) ;
#5237=CARTESIAN_POINT ( 'NONE',  ( 2.500000000000000000, 2.500728763858895382E-16, -2.041999999999999815 ) ) ;
#5247=VERTEX_POINT ( 'NONE', #10277 ) ;
#5262=AXIS2_PLACEMENT_3D ( 'NONE', #6725, #5388, #11290 ) ;
#5270=VERTEX_POINT ( 'NONE', #12695 ) ;
#5304=DIRECTION ( 'NONE',  ( 0.000000000000000000, 0.000000000000000000, 1.000000000000000000 ) ) ;
#5306=DIRECTION ( 'NONE',  ( 0.000000000000000000, -1.000000000000000000, 1.287488025362403787E-15 ) ) ;
#5331=DIRECTION ( 'NONE',  ( 0.000000000000000000, 0.000000000000000000, 1.000000000000000000 ) ) ;
#5379=DIRECTION ( 'NONE',  ( 0.000000000000000000, -0.4999999999999993339, 0.8660254037844390407 ) ) ;
#5388=DIRECTION ( 'NONE',  ( 0.000000000000000000, -1.000000000000000000, 0.000000000000000000 ) ) ;
#5401=CARTESIAN_POINT ( 'NONE',  ( 20.55500000000001748, 0.000000000000000000, 2.500000000000000888 ) ) ;
#5420=DIRECTION ( 'NONE',  ( -1.000000000000000000, -0.000000000000000000, -0.000000000000000000 ) ) ;
#5501=ADVANCED_FACE ( 'NONE', ( #2456 ), #11179, .F. ) ;
#5503=ORIENTED_EDGE ( 'NONE', *, *, #7484, .T. ) ;
#5511=PLANE ( 'NONE',  #13605 ) ;
#5538=FACE_OUTER_BOUND ( 'NONE', #8958, .T. ) ;
#5543=AXIS2_PLACEMENT_3D ( 'NONE', #14403, #1362, #15926 ) ;
#5602=ORIENTED_EDGE ( 'NONE', *, *, #8999, .T. ) ;
#5615=DIRECTION ( 'NONE',  ( -1.000000000000000000, -0.000000000000000000, -0.000000000000000000 ) ) ;
#5620=DIRECTION ( 'NONE',  ( 0.000000000000000000, 0.000000000000000000, -1.000000000000000000 ) ) ;
#5622=EDGE_CURVE ( 'NONE', #3664, #2762, #9047, .T. ) ;
#5625=ADVANCED_FACE ( 'NONE', ( #159 ), #18730, .T. ) ;
#5690=DIRECTION ( 'NONE',  ( 1.000000000000000000, 0.000000000000000000, 0.000000000000000000 ) ) ;
#5692=EDGE_LOOP ( 'NONE', ( #14446, #6636, #16443 ) ) ;
#5715=CARTESIAN_POINT ( 'NONE',  ( 5.200000000000002842, 3.061616997868383634E-16, -2.500000000000000444 ) ) ;
#5757=ADVANCED_FACE ( 'NONE', ( #13404 ), #6435, .T. ) ;
#5766=DIRECTION ( 'NONE',  ( 0.000000000000000000, 0.4999999999999990008, -0.8660254037844391517 ) ) ;
#5775=VERTEX_POINT ( 'NONE', #349 ) ;
#5827=VECTOR ( 'NONE', #8470, 1000.000000000000000 ) ;
#5832=DIRECTION ( 'NONE',  ( 0.000000000000000000, 0.000000000000000000, 1.000000000000000000 ) ) ;
#5837=SHAPE_DEFINITION_REPRESENTATION ( #17121, #8256 ) ;
#5877=DIRECTION ( 'NONE',  ( 0.000000000000000000, -0.8660254037844390407, -0.4999999999999993339 ) ) ;
#5892=CARTESIAN_POINT ( 'NONE',  ( 0.000000000000000000, 0.000000000000000000, 0.000000000000000000 ) ) ;
#5899=LINE ( 'NONE', #11712, #13870 ) ;
#5918=EDGE_CURVE ( 'NONE', #1626, #10049, #15575, .T. ) ;
#5925=AXIS2_PLACEMENT_3D ( 'NONE', #15881, #232, #6034 ) ;
#5936=CARTESIAN_POINT ( 'NONE',  ( 2.500000000000000000, -1.178949249685218748, -2.041999999999998039 ) ) ;
#5974=AXIS2_PLACEMENT_3D ( 'NONE', #1974, #12072, #11883 ) ;
#5979=CIRCLE ( 'NONE', #15734, 2.500000000000000888 ) ;
#5989=DIRECTION ( 'NONE',  ( 0.000000000000000000, 1.000000000000000000, -1.287488025362403787E-15 ) ) ;
#5991=CARTESIAN_POINT ( 'NONE',  ( 21.00000000000000355, 0.000000000000000000, 2.055000000000000160 ) ) ;
#6009=DIRECTION ( 'NONE',  ( 0.000000000000000000, 0.000000000000000000, 1.000000000000000000 ) ) ;
#6034=DIRECTION ( 'NONE',  ( 0.000000000000000000, 0.000000000000000000, 1.000000000000000000 ) ) ;
#6054=CARTESIAN_POINT ( 'NONE',  ( 2.500000000000000000, -1.178949249685214307, 2.042000000000001592 ) ) ;
#6099=CARTESIAN_POINT ( 'NONE',  ( 2.500000000000000000, -1.178949249685214307, 2.042000000000001592 ) ) ;
#6132=LINE ( 'NONE', #10420, #13014 ) ;
#6169=DIRECTION ( 'NONE',  ( 0.000000000000000000, 0.000000000000000000, -1.000000000000000000 ) ) ;
#6171=ORIENTED_EDGE ( 'NONE', *, *, #9344, .F. ) ;
#6176=PLANE ( 'NONE',  #11135 ) ;
#6190=ADVANCED_FACE ( 'NONE', ( #3374 ), #10330, .T. ) ;
#6219=CARTESIAN_POINT ( 'NONE',  ( -31.74999999999995737, 0.000000000000000000, 0.000000000000000000 ) ) ;
#6233=CIRCLE ( 'NONE', #17780, 0.2500000000000002220 ) ;
#6262=DIRECTION ( 'NONE',  ( 0.000000000000000000, -1.224646799147353454E-16, 1.000000000000000000 ) ) ;
#6265=VERTEX_POINT ( 'NONE', #7560 ) ;
#6268=AXIS2_PLACEMENT_3D ( 'NONE', #6312, #9353, #16790 ) ;
#6272=DIRECTION ( 'NONE',  ( 0.000000000000000000, 0.000000000000000000, -1.000000000000000000 ) ) ;
#6306=ORIENTED_EDGE ( 'NONE', *, *, #13437, .T. ) ;
#6312=CARTESIAN_POINT ( 'NONE',  ( 2.500000000000000000, 2.357898499370431722, -2.818925648462311528E-15 ) ) ;
#6320=ORIENTED_EDGE ( 'NONE', *, *, #17413, .F. ) ;
#6435=CYLINDRICAL_SURFACE ( 'NONE', #1752, 2.500000000000000444 ) ;
#6453=DIRECTION ( 'NONE',  ( 0.000000000000000000, 0.000000000000000000, 1.000000000000000000 ) ) ;
#6461=EDGE_CURVE ( 'NONE', #7707, #2698, #15497, .T. ) ;
#6467=VECTOR ( 'NONE', #14946, 1000.000000000000000 ) ;
#6535=CARTESIAN_POINT ( 'NONE',  ( 0.000000000000000000, -1.178949249685214307, 2.042000000000001592 ) ) ;
#6578=CARTESIAN_POINT ( 'NONE',  ( 0.2500000000000002220, 0.000000000000000000, 0.000000000000000000 ) ) ;
#6604=ORIENTED_EDGE ( 'NONE', *, *, #13437, .F. ) ;
#6636=ORIENTED_EDGE ( 'NONE', *, *, #16162, .F. ) ;
#6641=EDGE_CURVE ( 'NONE', #4599, #2059, #2098, .T. ) ;
#6725=CARTESIAN_POINT ( 'NONE',  ( 5.200000000000002842, 0.000000000000000000, -2.700000000000000622 ) ) ;
#6730=VERTEX_POINT ( 'NONE', #15163 ) ;
#6744=FACE_OUTER_BOUND ( 'NONE', #18600, .T. ) ;
#6847=ADVANCED_FACE ( 'NONE', ( #1344 ), #12578, .F. ) ;
#6861=LINE ( 'NONE', #1348, #14867 ) ;
#6889=CIRCLE ( 'NONE', #1122, 2.500000000000000444 ) ;
#6897=( GEOMETRIC_REPRESENTATION_CONTEXT ( 3 ) GLOBAL_UNCERTAINTY_ASSIGNED_CONTEXT ( ( #11083 ) ) GLOBAL_UNIT_ASSIGNED_CONTEXT ( ( #16851, #15422, #13994 ) ) REPRESENTATION_CONTEXT ( 'NONE', 'WORKASPACE' ) );
#6902=CARTESIAN_POINT ( 'NONE',  ( 2.500000000000000000, 2.357898499370431722, -2.818925648462311528E-15 ) ) ;
#6907=VERTEX_POINT ( 'NONE', #18766 ) ;
#6915=SURFACE_SIDE_STYLE ('',( #18629 ) ) ;
#6951=CIRCLE ( 'NONE', #8487, 2.700000000000000622 ) ;
#6954=AXIS2_PLACEMENT_3D ( 'NONE', #6219, #3278, #17567 ) ;
#6955=ORIENTED_EDGE ( 'NONE', *, *, #6641, .F. ) ;
#7001=PLANE ( 'NONE',  #933 ) ;
#7014=CARTESIAN_POINT ( 'NONE',  ( 2.500000000000000000, -1.768423874527823569, 1.021000000000002350 ) ) ;
#7030=CARTESIAN_POINT ( 'NONE',  ( 2.500000000000000000, 2.357898499370431722, -2.818925648462311528E-15 ) ) ;
#7062=FACE_OUTER_BOUND ( 'NONE', #14190, .T. ) ;
#7077=VECTOR ( 'NONE', #15695, 1000.000000000000000 ) ;
#7104=UNCERTAINTY_MEASURE_WITH_UNIT (LENGTH_MEASURE( 1.000000000000000082E-05 ), #11384, 'distance_accuracy_value', 'NONE');
#7119=EDGE_CURVE ( 'NONE', #9531, #13493, #193, .T. ) ;
#7134=ORIENTED_EDGE ( 'NONE', *, *, #4575, .T. ) ;
#7181=ORIENTED_EDGE ( 'NONE', *, *, #9130, .F. ) ;
#7182=CARTESIAN_POINT ( 'NONE',  ( -31.74999999999995737, 3.061616997868383634E-16, -2.500000000000000444 ) ) ;
#7221=FACE_OUTER_BOUND ( 'NONE', #4555, .T. ) ;
#7228=CARTESIAN_POINT ( 'NONE',  ( 2.500000000000000000, 2.357898499370431722, -2.818925648462311528E-15 ) ) ;
#7273=AXIS2_PLACEMENT_3D ( 'NONE', #7030, #5877, #13031 ) ;
#7289=EDGE_LOOP ( 'NONE', ( #6171, #4281 ) ) ;
#7314=VERTEX_POINT ( 'NONE', #5936 ) ;
#7323=ORIENTED_EDGE ( 'NONE', *, *, #2362, .F. ) ;
#7340=CARTESIAN_POINT ( 'NONE',  ( 0.000000000000000000, 2.357898499370431722, -2.818925648462311528E-15 ) ) ;
#7430=( GEOMETRIC_REPRESENTATION_CONTEXT ( 3 ) GLOBAL_UNCERTAINTY_ASSIGNED_CONTEXT ( ( #254 ) ) GLOBAL_UNIT_ASSIGNED_CONTEXT ( ( #934, #2627, #11002 ) ) REPRESENTATION_CONTEXT ( 'NONE', 'WORKASPACE' ) );
#7481=PRODUCT_DEFINITION_CONTEXT ( 'detailed design', #8877, 'design' ) ;
#7484=EDGE_CURVE ( 'NONE', #3414, #9474, #2353, .T. ) ;
#7498=EDGE_CURVE ( 'NONE', #18077, #6730, #6132, .T. ) ;
#7545=ORIENTED_EDGE ( 'NONE', *, *, #18158, .F. ) ;
#7559=DIRECTION ( 'NONE',  ( -1.000000000000000000, -0.000000000000000000, -0.000000000000000000 ) ) ;
#7560=CARTESIAN_POINT ( 'NONE',  ( 0.000000000000000000, 1.178949249685217415, 2.041999999999998483 ) ) ;
#7596=EDGE_CURVE ( 'NONE', #1279, #18341, #18487, .T. ) ;
#7659=ADVANCED_FACE ( 'NONE', ( #3663 ), #3844, .F. ) ;
#7707=VERTEX_POINT ( 'NONE', #17457 ) ;
#7710=CARTESIAN_POINT ( 'NONE',  ( 2.500000000000000000, -2.629050547790028551E-15, -2.041999999999999815 ) ) ;
#7739=CARTESIAN_POINT ( 'NONE',  ( 2.500000000000000000, 0.000000000000000000, 0.000000000000000000 ) ) ;
#7748=AXIS2_PLACEMENT_3D ( 'NONE', #12074, #278, #6169 ) ;
#7758=DIRECTION ( 'NONE',  ( 0.000000000000000000, 0.000000000000000000, 1.000000000000000000 ) ) ;
#7765=CARTESIAN_POINT ( 'NONE',  ( 0.000000000000000000, -2.357898499370432166, 3.035766082959412415E-15 ) ) ;
#7768=DIRECTION ( 'NONE',  ( 0.000000000000000000, -1.000000000000000000, 1.287488025362403787E-15 ) ) ;
#7773=AXIS2_PLACEMENT_3D ( 'NONE', #10579, #14492, #6009 ) ;
#7795=ORIENTED_EDGE ( 'NONE', *, *, #13017, .F. ) ;
#7853=ORIENTED_EDGE ( 'NONE', *, *, #8548, .F. ) ;
#7929=CARTESIAN_POINT ( 'NONE',  ( 0.000000000000000000, 2.357898499370431722, -2.818925648462311528E-15 ) ) ;
#7934=DIRECTION ( 'NONE',  ( 0.000000000000000000, 0.000000000000000000, -1.000000000000000000 ) ) ;
#7961=ORIENTED_EDGE ( 'NONE', *, *, #18337, .T. ) ;
#8017=AXIS2_PLACEMENT_3D ( 'NONE', #12801, #14324, #9934 ) ;
#8026=CARTESIAN_POINT ( 'NONE',  ( 5.000000000000000888, 0.000000000000000000, 0.000000000000000000 ) ) ;
#8081=EDGE_LOOP ( 'NONE', ( #14207, #14077, #7961, #3395 ) ) ;
#8164=DIRECTION ( 'NONE',  ( 0.000000000000000000, 1.000000000000000000, -1.287488025362403787E-15 ) ) ;
#8237=DIRECTION ( 'NONE',  ( 0.000000000000000000, 1.224646799147353207E-16, 1.000000000000000000 ) ) ;
#8256=SHAPE_REPRESENTATION ( 'socket head cap screw_iso_ISO 4762 M5 x 16 - 16N', ( #8017 ), #7430 ) ;
#8258=FILL_AREA_STYLE_COLOUR ( '', #14143 ) ;
#8262=EDGE_CURVE ( 'NONE', #15093, #3414, #6861, .T. ) ;
#8269=ORIENTED_EDGE ( 'NONE', *, *, #17483, .T. ) ;
#8286=EDGE_LOOP ( 'NONE', ( #10468, #3915, #18260, #4539 ) ) ;
#8290=FACE_OUTER_BOUND ( 'NONE', #8979, .T. ) ;
#8297=ORIENTED_EDGE ( 'NONE', *, *, #13017, .T. ) ;
#8312=DIRECTION ( 'NONE',  ( 0.000000000000000000, -0.5000000000000013323, -0.8660254037844380415 ) ) ;
#8325=ADVANCED_FACE ( 'NONE', ( #16103, #16279 ), #3238, .T. ) ;
#8341=ORIENTED_EDGE ( 'NONE', *, *, #14602, .T. ) ;
#8372=MECHANICAL_DESIGN_GEOMETRIC_PRESENTATION_REPRESENTATION('',(#18083),#16573);
#8378=ORIENTED_EDGE ( 'NONE', *, *, #12573, .T. ) ;
#8379=DIRECTION ( 'NONE',  ( -1.000000000000000000, 0.000000000000000000, -0.000000000000000000 ) ) ;
#8451=DIRECTION ( 'NONE',  ( 0.000000000000000000, 0.000000000000000000, 1.000000000000000000 ) ) ;
#8470=DIRECTION ( 'NONE',  ( -1.000000000000000000, -0.000000000000000000, -0.000000000000000000 ) ) ;
#8487=AXIS2_PLACEMENT_3D ( 'NONE', #14567, #11535, #17153 ) ;
#8497=ORIENTED_EDGE ( 'NONE', *, *, #15242, .F. ) ;
#8511=EDGE_LOOP ( 'NONE', ( #916, #9093, #16933, #3473 ) ) ;
#8548=EDGE_CURVE ( 'NONE', #3664, #16857, #10606, .T. ) ;
#8563=CARTESIAN_POINT ( 'NONE',  ( 5.200000000000002842, 0.000000000000000000, 0.000000000000000000 ) ) ;
#8571=LINE ( 'NONE', #5237, #12540 ) ;
#8594=ADVANCED_FACE ( 'NONE', ( #10660 ), #1987, .T. ) ;
#8599=EDGE_CURVE ( 'NONE', #5775, #16191, #1671, .T. ) ;
#8697=AXIS2_PLACEMENT_3D ( 'NONE', #18128, #811, #8237 ) ;
#8776=LINE ( 'NONE', #7340, #18196 ) ;
#8792=EDGE_LOOP ( 'NONE', ( #554, #4064, #14674, #11854 ) ) ;
#8815=DIRECTION ( 'NONE',  ( 0.000000000000000000, -0.5000000000000009992, -0.8660254037844380415 ) ) ;
#8833=EDGE_LOOP ( 'NONE', ( #10066, #14124, #7181 ) ) ;
#8839=CARTESIAN_POINT ( 'NONE',  ( 0.2500000000000002220, 4.898587196589412829E-16, -4.000000000000000000 ) ) ;
#8856=DIRECTION ( 'NONE',  ( 0.000000000000000000, 0.5000000000000009992, 0.8660254037844380415 ) ) ;
#8861=CARTESIAN_POINT ( 'NONE',  ( 0.2500000000000002220, 0.000000000000000000, 0.000000000000000000 ) ) ;
#8862=CIRCLE ( 'NONE', #3715, 4.000000000000000000 ) ;
#8877=APPLICATION_CONTEXT ( 'automotive_design' ) ;
#8898=DIRECTION ( 'NONE',  ( -1.000000000000000000, -0.000000000000000000, -0.000000000000000000 ) ) ;
#8935=ORIENTED_EDGE ( 'NONE', *, *, #4492, .F. ) ;
#8947=ORIENTED_EDGE ( 'NONE', *, *, #3196, .T. ) ;
#8958=EDGE_LOOP ( 'NONE', ( #4338, #9791, #3128, #8269, #16866 ) ) ;
#8979=EDGE_LOOP ( 'NONE', ( #3903, #8378, #15833, #9962 ) ) ;
#8999=EDGE_CURVE ( 'NONE', #15225, #5247, #16637, .T. ) ;
#9047=CIRCLE ( 'NONE', #11791, 4.250000000000000000 ) ;
#9093=ORIENTED_EDGE ( 'NONE', *, *, #5622, .F. ) ;
#9107=CARTESIAN_POINT ( 'NONE',  ( 5.200000000000002842, 0.000000000000000000, 0.000000000000000000 ) ) ;
#9121=EDGE_CURVE ( 'NONE', #3414, #752, #17119, .T. ) ;
#9130=EDGE_CURVE ( 'NONE', #2059, #10049, #1509, .T. ) ;
#9181=LINE ( 'NONE', #4529, #17694 ) ;
#9265=DIRECTION ( 'NONE',  ( 0.000000000000000000, 0.000000000000000000, 1.000000000000000000 ) ) ;
#9344=EDGE_CURVE ( 'NONE', #9531, #18077, #12174, .T. ) ;
#9353=DIRECTION ( 'NONE',  ( 1.000000000000000000, 0.000000000000000000, 0.000000000000000000 ) ) ;
#9405=VECTOR ( 'NONE', #11811, 1000.000000000000114 ) ;
#9409=CARTESIAN_POINT ( 'NONE',  ( 2.500000000000000000, 0.000000000000000000, 0.000000000000000000 ) ) ;
#9447=DIRECTION ( 'NONE',  ( -1.000000000000000000, -0.000000000000000000, -0.000000000000000000 ) ) ;
#9474=VERTEX_POINT ( 'NONE', #17013 ) ;
#9495=ADVANCED_FACE ( 'NONE', ( #2611 ), #7001, .F. ) ;
#9510=ORIENTED_EDGE ( 'NONE', *, *, #2166, .F. ) ;
#9531=VERTEX_POINT ( 'NONE', #13000 ) ;
#9677=( NAMED_UNIT ( * ) PLANE_ANGLE_UNIT ( ) SI_UNIT ( $, .RADIAN. ) );
#9693=DIRECTION ( 'NONE',  ( -1.000000000000000000, -0.000000000000000000, -0.000000000000000000 ) ) ;
#9698=LINE ( 'NONE', #15318, #12740 ) ;
#9708=LINE ( 'NONE', #4092, #5827 ) ;
#9714=VECTOR ( 'NONE', #8164, 1000.000000000000000 ) ;
#9715=EDGE_CURVE ( 'NONE', #13493, #5775, #13823, .T. ) ;
#9745=CARTESIAN_POINT ( 'NONE',  ( 0.000000000000000000, 0.000000000000000000, 4.000000000000000000 ) ) ;
#9791=ORIENTED_EDGE ( 'NONE', *, *, #17413, .T. ) ;
#9902=DIRECTION ( 'NONE',  ( 0.000000000000000000, 0.000000000000000000, 1.000000000000000000 ) ) ;
#9907=AXIS2_PLACEMENT_3D ( 'NONE', #17724, #17812, #122 ) ;
#9926=CIRCLE ( 'NONE', #8697, 0.2000000000000000944 ) ;
#9934=DIRECTION ( 'NONE',  ( 1.000000000000000000, 0.000000000000000000, 0.000000000000000000 ) ) ;
#9945=CONICAL_SURFACE ( 'NONE', #1726, 2.055000000000000160, 0.7853981633974639331 ) ;
#9952=LINE ( 'NONE', #15767, #3974 ) ;
#9962=ORIENTED_EDGE ( 'NONE', *, *, #5033, .F. ) ;
#10049=VERTEX_POINT ( 'NONE', #10665 ) ;
#10066=ORIENTED_EDGE ( 'NONE', *, *, #10684, .T. ) ;
#10094=DIRECTION ( 'NONE',  ( 0.000000000000000000, 0.000000000000000000, -1.000000000000000000 ) ) ;
#10141=DIRECTION ( 'NONE',  ( -1.000000000000000000, -0.000000000000000000, -0.000000000000000000 ) ) ;
#10163=CARTESIAN_POINT ( 'NONE',  ( 0.2500000000000002220, 5.204748896376250699E-16, -4.250000000000000000 ) ) ;
#10166=VERTEX_POINT ( 'NONE', #6535 ) ;
#10208=DIRECTION ( 'NONE',  ( 0.000000000000000000, 0.000000000000000000, 1.000000000000000000 ) ) ;
#10238=LINE ( 'NONE', #4161, #180 ) ;
#10277=CARTESIAN_POINT ( 'NONE',  ( 0.000000000000000000, -1.178949249685218748, -2.041999999999998039 ) ) ;
#10330=CYLINDRICAL_SURFACE ( 'NONE', #6954, 4.250000000000000000 ) ;
#10383=FACE_OUTER_BOUND ( 'NONE', #13524, .T. ) ;
#10420=CARTESIAN_POINT ( 'NONE',  ( 21.00000000000000355, 2.516649172247811061E-16, -2.055000000000000160 ) ) ;
#10468=ORIENTED_EDGE ( 'NONE', *, *, #3196, .F. ) ;
#10569=EDGE_CURVE ( 'NONE', #10049, #7314, #11375, .T. ) ;
#10575=AXIS2_PLACEMENT_3D ( 'NONE', #2420, #16799, #7934 ) ;
#10579=CARTESIAN_POINT ( 'NONE',  ( 21.00000000000000355, 0.000000000000000000, 0.000000000000000000 ) ) ;
#10606=CIRCLE ( 'NONE', #17600, 0.2500000000000002220 ) ;
#10638=CARTESIAN_POINT ( 'NONE',  ( 0.000000000000000000, 1.178949249685212974, -2.042000000000001148 ) ) ;
#10660=FACE_OUTER_BOUND ( 'NONE', #8081, .T. ) ;
#10665=CARTESIAN_POINT ( 'NONE',  ( 2.500000000000000000, -1.768423874527825568, -1.020999999999998575 ) ) ;
#10684=EDGE_CURVE ( 'NONE', #2059, #7314, #9952, .T. ) ;
#10754=CARTESIAN_POINT ( 'NONE',  ( -31.74999999999995737, 5.204748896376250699E-16, -4.250000000000000000 ) ) ;
#10815=AXIS2_PLACEMENT_3D ( 'NONE', #969, #18483, #5331 ) ;
#10838=STYLED_ITEM('',(#18883),#3805);
#10862=ADVANCED_FACE ( 'NONE', ( #2211 ), #15261, .F. ) ;
#10878=DIRECTION ( 'NONE',  ( 0.000000000000000000, -0.4999999999999993339, 0.8660254037844390407 ) ) ;
#10918=AXIS2_PLACEMENT_3D ( 'NONE', #666, #570, #12187 ) ;
#10972=ORIENTED_EDGE ( 'NONE', *, *, #2863, .F. ) ;
#10983=EDGE_LOOP ( 'NONE', ( #9510, #4996, #13453, #7853 ) ) ;
#11002=( NAMED_UNIT ( * ) SI_UNIT ( $, .STERADIAN. ) SOLID_ANGLE_UNIT ( ) );
#11020=DIRECTION ( 'NONE',  ( -0.5000000000000051070, 0.000000000000000000, 0.8660254037844355990 ) ) ;
#11021=CARTESIAN_POINT ( 'NONE',  ( 2.500000000000000000, 1.178949249685212974, -2.042000000000001148 ) ) ;
#11026=ORIENTED_EDGE ( 'NONE', *, *, #7119, .F. ) ;
#11027=DIRECTION ( 'NONE',  ( 0.000000000000000000, 0.000000000000000000, -1.000000000000000000 ) ) ;
#11035=VERTEX_POINT ( 'NONE', #15837 ) ;
#11083=UNCERTAINTY_MEASURE_WITH_UNIT (LENGTH_MEASURE( 1.000000000000000082E-05 ), #16851, 'distance_accuracy_value', 'NONE');
#11092=ORIENTED_EDGE ( 'NONE', *, *, #14885, .F. ) ;
#11135=AXIS2_PLACEMENT_3D ( 'NONE', #17897, #11980, #6272 ) ;
#11136=DIRECTION ( 'NONE',  ( -1.000000000000000000, -0.000000000000000000, -0.000000000000000000 ) ) ;
#11170=DIRECTION ( 'NONE',  ( -0.000000000000000000, 0.8660254037844392627, 0.4999999999999990008 ) ) ;
#11172=ORIENTED_EDGE ( 'NONE', *, *, #4575, .F. ) ;
#11176=ADVANCED_FACE ( 'NONE', ( #1541 ), #12664, .T. ) ;
#11179=CONICAL_SURFACE ( 'NONE', #16363, 2.041999999999999815, 1.047197551196591858 ) ;
#11181=VECTOR ( 'NONE', #5379, 1000.000000000000000 ) ;
#11290=DIRECTION ( 'NONE',  ( 0.000000000000000000, 0.000000000000000000, -1.000000000000000000 ) ) ;
#11330=DIRECTION ( 'NONE',  ( 0.000000000000000000, -0.5000000000000009992, -0.8660254037844380415 ) ) ;
#11352=CARTESIAN_POINT ( 'NONE',  ( 2.500000000000000000, 2.357898499370431722, -2.818925648462311528E-15 ) ) ;
#11375=LINE ( 'NONE', #1103, #4011 ) ;
#11384=( LENGTH_UNIT ( ) NAMED_UNIT ( * ) SI_UNIT ( .MILLI., .METRE. ) );
#11410=DIRECTION ( 'NONE',  ( 0.000000000000000000, -0.5000000000000013323, -0.8660254037844380415 ) ) ;
#11419=DIRECTION ( 'NONE',  ( -0.000000000000000000, 0.000000000000000000, 1.000000000000000000 ) ) ;
#11422=DIRECTION ( 'NONE',  ( 0.000000000000000000, 0.000000000000000000, 1.000000000000000000 ) ) ;
#11442=CONICAL_SURFACE ( 'NONE', #10815, 2.041999999999999815, 1.047197551196591858 ) ;
#11443=EDGE_LOOP ( 'NONE', ( #15917, #8947, #2201, #3825 ) ) ;
#11447=DIRECTION ( 'NONE',  ( 0.000000000000000000, -0.5000000000000013323, -0.8660254037844380415 ) ) ;
#11457=DIRECTION ( 'NONE',  ( -1.000000000000000000, -0.000000000000000000, -0.000000000000000000 ) ) ;
#11477=AXIS2_PLACEMENT_3D ( 'NONE', #2635, #1124, #8451 ) ;
#11535=DIRECTION ( 'NONE',  ( -1.000000000000000000, -0.000000000000000000, -0.000000000000000000 ) ) ;
#11558=ORIENTED_EDGE ( 'NONE', *, *, #6641, .T. ) ;
#11574=ADVANCED_FACE ( 'NONE', ( #8290 ), #9945, .T. ) ;
#11594=PLANE ( 'NONE',  #16056 ) ;
#11619=DIRECTION ( 'NONE',  ( 1.000000000000000000, 0.000000000000000000, 0.000000000000000000 ) ) ;
#11630=DIRECTION ( 'NONE',  ( -1.000000000000000000, -0.000000000000000000, -0.000000000000000000 ) ) ;
#11659=VECTOR ( 'NONE', #17199, 1000.000000000000000 ) ;
#11712=CARTESIAN_POINT ( 'NONE',  ( 0.000000000000000000, -1.178949249685214307, 2.042000000000001592 ) ) ;
#11728=CIRCLE ( 'NONE', #7773, 2.055000000000000160 ) ;
#11770=CIRCLE ( 'NONE', #11477, 2.041999999999999815 ) ;
#11771=AXIS2_PLACEMENT_3D ( 'NONE', #7228, #11619, #10094 ) ;
#11791=AXIS2_PLACEMENT_3D ( 'NONE', #18640, #2830, #16070 ) ;
#11804=ORIENTED_EDGE ( 'NONE', *, *, #7484, .F. ) ;
#11811=DIRECTION ( 'NONE',  ( -0.7071067811865364705, 0.000000000000000000, 0.7071067811865584529 ) ) ;
#11824=ORIENTED_EDGE ( 'NONE', *, *, #17289, .T. ) ;
#11854=ORIENTED_EDGE ( 'NONE', *, *, #18337, .F. ) ;
#11872=DIRECTION ( 'NONE',  ( 0.000000000000000000, 0.000000000000000000, -1.000000000000000000 ) ) ;
#11883=DIRECTION ( 'NONE',  ( 0.000000000000000000, 0.000000000000000000, 1.000000000000000000 ) ) ;
#11925=ADVANCED_FACE ( 'NONE', ( #6744 ), #5511, .F. ) ;
#11980=DIRECTION ( 'NONE',  ( 1.000000000000000000, 0.000000000000000000, 0.000000000000000000 ) ) ;
#12045=CARTESIAN_POINT ( 'NONE',  ( 0.000000000000000000, 1.178949249685212974, -2.042000000000001148 ) ) ;
#12072=DIRECTION ( 'NONE',  ( -1.000000000000000000, -0.000000000000000000, -0.000000000000000000 ) ) ;
#12074=CARTESIAN_POINT ( 'NONE',  ( 2.500000000000000000, 2.357898499370431722, -2.818925648462311528E-15 ) ) ;
#12086=CARTESIAN_POINT ( 'NONE',  ( 5.000000000000000888, 4.250000000000000000, 0.000000000000000000 ) ) ;
#12094=EDGE_CURVE ( 'NONE', #16857, #11035, #473, .T. ) ;
#12096=ORIENTED_EDGE ( 'NONE', *, *, #14553, .F. ) ;
#12104=CIRCLE ( 'NONE', #12424, 4.250000000000000000 ) ;
#12137=ADVANCED_FACE ( 'NONE', ( #16319 ), #18732, .T. ) ;
#12144=AXIS2_PLACEMENT_3D ( 'NONE', #14681, #14771, #10208 ) ;
#12174=CIRCLE ( 'NONE', #602, 2.055000000000000160 ) ;
#12179=ORIENTED_EDGE ( 'NONE', *, *, #13205, .F. ) ;
#12187=DIRECTION ( 'NONE',  ( 0.000000000000000000, 0.000000000000000000, -1.000000000000000000 ) ) ;
#12238=VECTOR ( 'NONE', #14613, 1000.000000000000114 ) ;
#12251=CIRCLE ( 'NONE', #5262, 0.2000000000000000944 ) ;
#12252=EDGE_CURVE ( 'NONE', #6907, #6265, #5071, .T. ) ;
#12325=LINE ( 'NONE', #6902, #11181 ) ;
#12361=FACE_OUTER_BOUND ( 'NONE', #4680, .T. ) ;
#12371=AXIS2_PLACEMENT_3D ( 'NONE', #5892, #8379, #11419 ) ;
#12424=AXIS2_PLACEMENT_3D ( 'NONE', #6578, #3921, #18376 ) ;
#12467=ORIENTED_EDGE ( 'NONE', *, *, #15884, .F. ) ;
#12468=EDGE_LOOP ( 'NONE', ( #8497, #1282, #158 ) ) ;
#12471=DIRECTION ( 'NONE',  ( 0.000000000000000000, -1.000000000000000000, 0.000000000000000000 ) ) ;
#12509=ADVANCED_FACE ( 'NONE', ( #2984 ), #479, .T. ) ;
#12520=TOROIDAL_SURFACE ( 'NONE', #5543, 2.700000000000000622, 0.2000000000000000111 ) ;
#12536=PRESENTATION_STYLE_ASSIGNMENT (( #14152 ) ) ;
#12540=VECTOR ( 'NONE', #15723, 1000.000000000000114 ) ;
#12541=DIRECTION ( 'NONE',  ( 0.000000000000000000, 0.4999999999999990008, -0.8660254037844391517 ) ) ;
#12573=EDGE_CURVE ( 'NONE', #18077, #9531, #11728, .T. ) ;
#12578=PLANE ( 'NONE',  #13077 ) ;
#12664=TOROIDAL_SURFACE ( 'NONE', #13273, 4.000000000000000000, 0.2500000000000000000 ) ;
#12695=CARTESIAN_POINT ( 'NONE',  ( 3.678949249685231848, 0.000000000000000000, 0.000000000000000000 ) ) ;
#12740=VECTOR ( 'NONE', #11020, 1000.000000000000114 ) ;
#12777=CARTESIAN_POINT ( 'NONE',  ( 2.500000000000000000, 2.357898499370431722, -2.818925648462311528E-15 ) ) ;
#12786=LINE ( 'NONE', #11352, #16956 ) ;
#12801=CARTESIAN_POINT ( 'NONE',  ( 0.000000000000000000, 0.000000000000000000, 0.000000000000000000 ) ) ;
#12847=ORIENTED_EDGE ( 'NONE', *, *, #476, .F. ) ;
#12866=FACE_OUTER_BOUND ( 'NONE', #12468, .T. ) ;
#12881=ADVANCED_FACE ( 'NONE', ( #5538 ), #11442, .F. ) ;
#12885=PLANE ( 'NONE',  #13607 ) ;
#13000=CARTESIAN_POINT ( 'NONE',  ( 21.00000000000000355, 0.000000000000000000, 2.055000000000000160 ) ) ;
#13014=VECTOR ( 'NONE', #612, 1000.000000000000114 ) ;
#13017=EDGE_CURVE ( 'NONE', #10166, #6265, #5899, .T. ) ;
#13031=DIRECTION ( 'NONE',  ( 0.000000000000000000, 0.4999999999999992784, -0.8660254037844389297 ) ) ;
#13077=AXIS2_PLACEMENT_3D ( 'NONE', #12777, #1059, #5620 ) ;
#13084=ADVANCED_FACE ( 'NONE', ( #12361 ), #6176, .F. ) ;
#13097=DIRECTION ( 'NONE',  ( 0.000000000000000000, 0.5000000000000011102, 0.8660254037844379305 ) ) ;
#13205=EDGE_CURVE ( 'NONE', #15093, #13701, #14916, .T. ) ;
#13273=AXIS2_PLACEMENT_3D ( 'NONE', #8861, #2978, #13356 ) ;
#13276=VECTOR ( 'NONE', #8312, 999.9999999999997726 ) ;
#13310=CIRCLE ( 'NONE', #15745, 2.041999999999999815 ) ;
#13356=DIRECTION ( 'NONE',  ( 0.000000000000000000, 0.000000000000000000, 1.000000000000000000 ) ) ;
#13375=CARTESIAN_POINT ( 'NONE',  ( 2.500000000000000000, 1.178949249685212974, -2.042000000000001148 ) ) ;
#13397=CARTESIAN_POINT ( 'NONE',  ( 2.500000000000000000, -1.178949249685214307, 2.042000000000001592 ) ) ;
#13404=FACE_OUTER_BOUND ( 'NONE', #8286, .T. ) ;
#13437=EDGE_CURVE ( 'NONE', #4084, #5247, #939, .T. ) ;
#13453=ORIENTED_EDGE ( 'NONE', *, *, #12094, .F. ) ;
#13479=EDGE_LOOP ( 'NONE', ( #15801, #2207, #4259, #12096, #18235 ) ) ;
#13480=CIRCLE ( 'NONE', #15910, 4.250000000000000000 ) ;
#13493=VERTEX_POINT ( 'NONE', #5401 ) ;
#13494=DIRECTION ( 'NONE',  ( -1.000000000000000000, -0.000000000000000000, -0.000000000000000000 ) ) ;
#13524=EDGE_LOOP ( 'NONE', ( #3750, #14596, #15938, #11026 ) ) ;
#13605=AXIS2_PLACEMENT_3D ( 'NONE', #1035, #18357, #5306 ) ;
#13607=AXIS2_PLACEMENT_3D ( 'NONE', #6099, #14671, #8856 ) ;
#13662=AXIS2_PLACEMENT_3D ( 'NONE', #862, #762, #18277 ) ;
#13701=VERTEX_POINT ( 'NONE', #7014 ) ;
#13749=EDGE_LOOP ( 'NONE', ( #16757, #14009 ) ) ;
#13756=TOROIDAL_SURFACE ( 'NONE', #2495, 2.700000000000000622, 0.2000000000000000111 ) ;
#13765=ORIENTED_EDGE ( 'NONE', *, *, #2610, .T. ) ;
#13823=LINE ( 'NONE', #4883, #30 ) ;
#13870=VECTOR ( 'NONE', #5989, 1000.000000000000000 ) ;
#13929=AXIS2_PLACEMENT_3D ( 'NONE', #8026, #4979, #18315 ) ;
#13972=FILL_AREA_STYLE ('',( #8258 ) ) ;
#13994=( NAMED_UNIT ( * ) SI_UNIT ( $, .STERADIAN. ) SOLID_ANGLE_UNIT ( ) );
#14009=ORIENTED_EDGE ( 'NONE', *, *, #2362, .T. ) ;
#14013=CARTESIAN_POINT ( 'NONE',  ( 2.500000000000000000, 2.629050547790028946E-15, 2.042000000000000259 ) ) ;
#14044=ORIENTED_EDGE ( 'NONE', *, *, #4492, .T. ) ;
#14061=( NAMED_UNIT ( * ) SI_UNIT ( $, .STERADIAN. ) SOLID_ANGLE_UNIT ( ) );
#14063=DIRECTION ( 'NONE',  ( -1.000000000000000000, -0.000000000000000000, -0.000000000000000000 ) ) ;
#14077=ORIENTED_EDGE ( 'NONE', *, *, #6461, .T. ) ;
#14078=CARTESIAN_POINT ( 'NONE',  ( 2.500000000000000000, -2.357898499370432166, 3.035766082959412415E-15 ) ) ;
#14124=ORIENTED_EDGE ( 'NONE', *, *, #10569, .F. ) ;
#14143=COLOUR_RGB ( '',1.000000000000000000, 0.9490196078431372140, 0.9098039215686274384 ) ;
#14152=SURFACE_STYLE_USAGE ( .BOTH. , #6915 ) ;
#14172=LINE ( 'NONE', #11021, #7077 ) ;
#14190=EDGE_LOOP ( 'NONE', ( #15258, #14926, #14341, #1934, #2972 ) ) ;
#14204=CIRCLE ( 'NONE', #5974, 2.500000000000000888 ) ;
#14207=ORIENTED_EDGE ( 'NONE', *, *, #966, .F. ) ;
#14292=VECTOR ( 'NONE', #7768, 1000.000000000000000 ) ;
#14304=DIRECTION ( 'NONE',  ( 0.000000000000000000, 1.000000000000000000, -1.287488025362403787E-15 ) ) ;
#14311=DIRECTION ( 'NONE',  ( 0.000000000000000000, -0.4999999999999993339, 0.8660254037844390407 ) ) ;
#14324=DIRECTION ( 'NONE',  ( 0.000000000000000000, 0.000000000000000000, 1.000000000000000000 ) ) ;
#14333=DIRECTION ( 'NONE',  ( 0.000000000000000000, -1.000000000000000000, 1.287488025362403787E-15 ) ) ;
#14341=ORIENTED_EDGE ( 'NONE', *, *, #13205, .T. ) ;
#14344=CARTESIAN_POINT ( 'NONE',  ( 2.500000000000000000, -1.178949249685214307, 2.042000000000001592 ) ) ;
#14403=CARTESIAN_POINT ( 'NONE',  ( 5.200000000000002842, 0.000000000000000000, 0.000000000000000000 ) ) ;
#14446=ORIENTED_EDGE ( 'NONE', *, *, #5918, .F. ) ;
#14492=DIRECTION ( 'NONE',  ( -1.000000000000000000, -0.000000000000000000, -0.000000000000000000 ) ) ;
#14517=LINE ( 'NONE', #1298, #11659 ) ;
#14553=EDGE_CURVE ( 'NONE', #17667, #4599, #17443, .T. ) ;
#14567=CARTESIAN_POINT ( 'NONE',  ( 5.000000000000000888, 0.000000000000000000, 0.000000000000000000 ) ) ;
#14571=ORIENTED_EDGE ( 'NONE', *, *, #18158, .T. ) ;
#14580=AXIS2_PLACEMENT_3D ( 'NONE', #2445, #14063, #1023 ) ;
#14596=ORIENTED_EDGE ( 'NONE', *, *, #7498, .T. ) ;
#14602=EDGE_CURVE ( 'NONE', #9474, #752, #12786, .T. ) ;
#14604=ADVANCED_FACE ( 'NONE', ( #7062 ), #12885, .T. ) ;
#14613=DIRECTION ( 'NONE',  ( 0.000000000000000000, -0.5000000000000009992, -0.8660254037844380415 ) ) ;
#14619=ORIENTED_EDGE ( 'NONE', *, *, #8999, .F. ) ;
#14629=DIRECTION ( 'NONE',  ( 0.000000000000000000, -1.287488025362403787E-15, -1.000000000000000000 ) ) ;
#14671=DIRECTION ( 'NONE',  ( 0.000000000000000000, 0.8660254037844380415, -0.5000000000000009992 ) ) ;
#14674=ORIENTED_EDGE ( 'NONE', *, *, #2166, .T. ) ;
#14681=CARTESIAN_POINT ( 'NONE',  ( 2.500000000000000000, 0.000000000000000000, 0.000000000000000000 ) ) ;
#14691=EDGE_CURVE ( 'NONE', #13493, #6730, #5979, .T. ) ;
#14757=ADVANCED_FACE ( 'NONE', ( #10383 ), #18156, .T. ) ;
#14771=DIRECTION ( 'NONE',  ( -1.000000000000000000, -0.000000000000000000, -0.000000000000000000 ) ) ;
#14867=VECTOR ( 'NONE', #14304, 1000.000000000000000 ) ;
#14885=EDGE_CURVE ( 'NONE', #13701, #3414, #11770, .T. ) ;
#14916=LINE ( 'NONE', #13397, #17487 ) ;
#14926=ORIENTED_EDGE ( 'NONE', *, *, #4357, .F. ) ;
#14946=DIRECTION ( 'NONE',  ( 0.000000000000000000, -1.000000000000000000, 1.287488025362403787E-15 ) ) ;
#14964=ADVANCED_FACE ( 'NONE', ( #2824 ), #11594, .F. ) ;
#14966=AXIS2_PLACEMENT_3D ( 'NONE', #1056, #4014, #9902 ) ;
#15040=CARTESIAN_POINT ( 'NONE',  ( 0.2500000000000002220, 0.000000000000000000, 4.250000000000000000 ) ) ;
#15093=VERTEX_POINT ( 'NONE', #6054 ) ;
#15151=EDGE_LOOP ( 'NONE', ( #6604, #2921, #4253, #3577, #17748 ) ) ;
#15163=CARTESIAN_POINT ( 'NONE',  ( 20.55500000000001748, 3.061616997868384127E-16, -2.500000000000000888 ) ) ;
#15184=AXIS2_PLACEMENT_3D ( 'NONE', #4318, #11457, #5832 ) ;
#15225=VERTEX_POINT ( 'NONE', #12045 ) ;
#15242=EDGE_CURVE ( 'NONE', #17667, #9474, #12325, .T. ) ;
#15258=ORIENTED_EDGE ( 'NONE', *, *, #16640, .F. ) ;
#15261=PLANE ( 'NONE',  #6268 ) ;
#15281=CARTESIAN_POINT ( 'NONE',  ( 21.00000000000000355, 0.000000000000000000, 0.000000000000000000 ) ) ;
#15306=EDGE_CURVE ( 'NONE', #9474, #4599, #13310, .T. ) ;
#15318=CARTESIAN_POINT ( 'NONE',  ( 2.500000000000000000, 0.000000000000000000, 2.041999999999999815 ) ) ;
#15422=( NAMED_UNIT ( * ) PLANE_ANGLE_UNIT ( ) SI_UNIT ( $, .RADIAN. ) );
#15424=CARTESIAN_POINT ( 'NONE',  ( 0.2500000000000002220, 0.000000000000000000, 4.000000000000000000 ) ) ;
#15497=CIRCLE ( 'NONE', #15184, 4.250000000000000000 ) ;
#15528=FACE_OUTER_BOUND ( 'NONE', #3005, .T. ) ;
#15575=LINE ( 'NONE', #924, #16062 ) ;
#15577=CIRCLE ( 'NONE', #14966, 2.041999999999999815 ) ;
#15630=PRODUCT_DEFINITION ( 'UNKNOWN', '', #18710, #7481 ) ;
#15674=VERTEX_POINT ( 'NONE', #13375 ) ;
#15695=DIRECTION ( 'NONE',  ( -1.000000000000000000, -0.000000000000000000, -0.000000000000000000 ) ) ;
#15723=DIRECTION ( 'NONE',  ( -0.5000000000000051070, 1.060575238724903217E-16, -0.8660254037844355990 ) ) ;
#15731=MECHANICAL_DESIGN_GEOMETRIC_PRESENTATION_REPRESENTATION('',(#10838),#6897);
#15733=ORIENTED_EDGE ( 'NONE', *, *, #177, .F. ) ;
#15734=AXIS2_PLACEMENT_3D ( 'NONE', #16110, #2973, #6453 ) ;
#15744=FACE_OUTER_BOUND ( 'NONE', #4184, .T. ) ;
#15745=AXIS2_PLACEMENT_3D ( 'NONE', #18241, #18528, #5091 ) ;
#15767=CARTESIAN_POINT ( 'NONE',  ( 2.500000000000000000, 1.178949249685212974, -2.042000000000001148 ) ) ;
#15796=DIRECTION ( 'NONE',  ( 0.000000000000000000, 0.000000000000000000, 1.000000000000000000 ) ) ;
#15801=ORIENTED_EDGE ( 'NONE', *, *, #15884, .T. ) ;
#15828=CARTESIAN_POINT ( 'NONE',  ( 4.999999999999997335, 0.000000000000000000, 0.000000000000000000 ) ) ;
#15833=ORIENTED_EDGE ( 'NONE', *, *, #7119, .T. ) ;
#15837=CARTESIAN_POINT ( 'NONE',  ( 0.000000000000000000, 5.051668046482832750E-16, -4.000000000000000000 ) ) ;
#15881=CARTESIAN_POINT ( 'NONE',  ( -31.74999999999995737, 0.000000000000000000, 0.000000000000000000 ) ) ;
#15883=ORIENTED_EDGE ( 'NONE', *, *, #6461, .F. ) ;
#15884=EDGE_CURVE ( 'NONE', #6907, #15225, #8776, .T. ) ;
#15910=AXIS2_PLACEMENT_3D ( 'NONE', #15828, #11630, #2777 ) ;
#15917=ORIENTED_EDGE ( 'NONE', *, *, #14691, .T. ) ;
#15926=DIRECTION ( 'NONE',  ( 0.000000000000000000, 0.000000000000000000, -1.000000000000000000 ) ) ;
#15938=ORIENTED_EDGE ( 'NONE', *, *, #14691, .F. ) ;
#15978=VECTOR ( 'NONE', #10878, 1000.000000000000000 ) ;
#15986=EDGE_LOOP ( 'NONE', ( #15733, #15883 ) ) ;
#16043=LINE ( 'NONE', #3003, #12238 ) ;
#16047=CARTESIAN_POINT ( 'NONE',  ( 5.000000000000002665, 3.306546357697854226E-16, 2.700000000000000622 ) ) ;
#16052=DIRECTION ( 'NONE',  ( -1.000000000000000000, -0.000000000000000000, -0.000000000000000000 ) ) ;
#16056=AXIS2_PLACEMENT_3D ( 'NONE', #1668, #14629, #4168 ) ;
#16062=VECTOR ( 'NONE', #1012, 1000.000000000000114 ) ;
#16070=DIRECTION ( 'NONE',  ( 0.000000000000000000, 0.000000000000000000, 1.000000000000000000 ) ) ;
#16103=FACE_BOUND ( 'NONE', #13749, .T. ) ;
#16110=CARTESIAN_POINT ( 'NONE',  ( 20.55500000000001748, 0.000000000000000000, 0.000000000000000000 ) ) ;
#16148=LINE ( 'NONE', #1755, #4444 ) ;
#16162=EDGE_CURVE ( 'NONE', #13701, #1626, #2563, .T. ) ;
#16178=PLANE ( 'NONE',  #7748 ) ;
#16191=VERTEX_POINT ( 'NONE', #5715 ) ;
#16197=CARTESIAN_POINT ( 'NONE',  ( 21.00000000000000355, 0.000000000000000000, 0.000000000000000000 ) ) ;
#16213=ORIENTED_EDGE ( 'NONE', *, *, #15242, .T. ) ;
#16241=ORIENTED_EDGE ( 'NONE', *, *, #12252, .T. ) ;
#16251=ADVANCED_FACE ( 'NONE', ( #4647 ), #16178, .F. ) ;
#16279=FACE_OUTER_BOUND ( 'NONE', #15986, .T. ) ;
#16319=FACE_OUTER_BOUND ( 'NONE', #11443, .T. ) ;
#16337=EDGE_CURVE ( 'NONE', #2762, #11035, #6233, .T. ) ;
#16355=EDGE_LOOP ( 'NONE', ( #16241, #7795, #16935, #6306, #14619, #12467 ) ) ;
#16363=AXIS2_PLACEMENT_3D ( 'NONE', #9409, #9693, #5304 ) ;
#16378=LINE ( 'NONE', #5017, #6467 ) ;
#16421=CARTESIAN_POINT ( 'NONE',  ( 0.000000000000000000, 0.000000000000000000, 0.000000000000000000 ) ) ;
#16437=DIRECTION ( 'NONE',  ( -1.000000000000000000, -0.000000000000000000, -0.000000000000000000 ) ) ;
#16443=ORIENTED_EDGE ( 'NONE', *, *, #17483, .F. ) ;
#16537=EDGE_LOOP ( 'NONE', ( #5602, #12847, #1479, #18332, #18089 ) ) ;
#16570=LINE ( 'NONE', #10754, #2949 ) ;
#16573=( GEOMETRIC_REPRESENTATION_CONTEXT ( 3 ) GLOBAL_UNCERTAINTY_ASSIGNED_CONTEXT ( ( #7104 ) ) GLOBAL_UNIT_ASSIGNED_CONTEXT ( ( #11384, #9677, #14061 ) ) REPRESENTATION_CONTEXT ( 'NONE', 'WORKASPACE' ) );
#16602=EDGE_LOOP ( 'NONE', ( #1410, #16758, #6955 ) ) ;
#16637=LINE ( 'NONE', #10638, #14292 ) ;
#16640=EDGE_CURVE ( 'NONE', #10166, #4084, #16043, .T. ) ;
#16656=LINE ( 'NONE', #14078, #4527 ) ;
#16757=ORIENTED_EDGE ( 'NONE', *, *, #7596, .T. ) ;
#16758=ORIENTED_EDGE ( 'NONE', *, *, #17728, .T. ) ;
#16790=DIRECTION ( 'NONE',  ( 0.000000000000000000, 0.000000000000000000, -1.000000000000000000 ) ) ;
#16798=FACE_OUTER_BOUND ( 'NONE', #15151, .T. ) ;
#16799=DIRECTION ( 'NONE',  ( 1.000000000000000000, 0.000000000000000000, 0.000000000000000000 ) ) ;
#16812=DIRECTION ( 'NONE',  ( 0.000000000000000000, 0.000000000000000000, 1.000000000000000000 ) ) ;
#16851=( LENGTH_UNIT ( ) NAMED_UNIT ( * ) SI_UNIT ( .MILLI., .METRE. ) );
#16857=VERTEX_POINT ( 'NONE', #9745 ) ;
#16866=ORIENTED_EDGE ( 'NONE', *, *, #14885, .T. ) ;
#16933=ORIENTED_EDGE ( 'NONE', *, *, #8548, .T. ) ;
#16935=ORIENTED_EDGE ( 'NONE', *, *, #16640, .T. ) ;
#16956=VECTOR ( 'NONE', #14311, 1000.000000000000000 ) ;
#17000=DIRECTION ( 'NONE',  ( 0.000000000000000000, -0.4999999999999989453, 0.8660254037844391517 ) ) ;
#17013=CARTESIAN_POINT ( 'NONE',  ( 2.500000000000000000, 1.768423874527823791, 1.020999999999998353 ) ) ;
#17085=ADVANCED_FACE ( 'NONE', ( #15744 ), #12520, .F. ) ;
#17119=LINE ( 'NONE', #14344, #9714 ) ;
#17121=PRODUCT_DEFINITION_SHAPE ( 'NONE', 'NONE',  #15630 ) ;
#17153=DIRECTION ( 'NONE',  ( 0.000000000000000000, 0.000000000000000000, -1.000000000000000000 ) ) ;
#17185=PRODUCT_CONTEXT ( 'NONE', #1708, 'mechanical' ) ;
#17199=DIRECTION ( 'NONE',  ( -1.000000000000000000, -0.000000000000000000, -0.000000000000000000 ) ) ;
#17223=FACE_OUTER_BOUND ( 'NONE', #4040, .T. ) ;
#17238=DIRECTION ( 'NONE',  ( -1.000000000000000000, -0.000000000000000000, -0.000000000000000000 ) ) ;
#17289=EDGE_CURVE ( 'NONE', #11035, #16857, #8862, .T. ) ;
#17315=AXIS2_PLACEMENT_3D ( 'NONE', #12086, #1530, #4854 ) ;
#17325=ADVANCED_FACE ( 'NONE', ( #7221 ), #13756, .F. ) ;
#17379=CARTESIAN_POINT ( 'NONE',  ( 2.500000000000000000, 2.357898499370431722, -2.818925648462311528E-15 ) ) ;
#17413=EDGE_CURVE ( 'NONE', #5270, #2059, #8571, .T. ) ;
#17443=LINE ( 'NONE', #4391, #13276 ) ;
#17457=CARTESIAN_POINT ( 'NONE',  ( 4.999999999999997335, 5.204748896376250699E-16, -4.250000000000000000 ) ) ;
#17483=EDGE_CURVE ( 'NONE', #10049, #13701, #15577, .T. ) ;
#17487=VECTOR ( 'NONE', #8815, 1000.000000000000114 ) ;
#17567=DIRECTION ( 'NONE',  ( 0.000000000000000000, 0.000000000000000000, 1.000000000000000000 ) ) ;
#17600=AXIS2_PLACEMENT_3D ( 'NONE', #15424, #12471, #11027 ) ;
#17667=VERTEX_POINT ( 'NONE', #3510 ) ;
#17694=VECTOR ( 'NONE', #11410, 999.9999999999997726 ) ;
#17724=CARTESIAN_POINT ( 'NONE',  ( 0.2500000000000002220, 0.000000000000000000, 0.000000000000000000 ) ) ;
#17728=EDGE_CURVE ( 'NONE', #15674, #2059, #16378, .T. ) ;
#17748=ORIENTED_EDGE ( 'NONE', *, *, #476, .T. ) ;
#17751=DIRECTION ( 'NONE',  ( -1.000000000000000000, -0.000000000000000000, -0.000000000000000000 ) ) ;
#17780=AXIS2_PLACEMENT_3D ( 'NONE', #8839, #183, #6262 ) ;
#17812=DIRECTION ( 'NONE',  ( -1.000000000000000000, -0.000000000000000000, -0.000000000000000000 ) ) ;
#17869=CARTESIAN_POINT ( 'NONE',  ( -31.74999999999995737, 0.000000000000000000, 0.000000000000000000 ) ) ;
#17897=CARTESIAN_POINT ( 'NONE',  ( 2.500000000000000000, 2.357898499370431722, -2.818925648462311528E-15 ) ) ;
#17907=EDGE_CURVE ( 'NONE', #15674, #15225, #14172, .T. ) ;
#17939=ORIENTED_EDGE ( 'NONE', *, *, #4357, .T. ) ;
#18036=CLOSED_SHELL ( 'NONE', ( #12881, #11176, #17085, #14757, #12137, #6190, #4857, #8594, #8325, #5757, #11574, #5625, #17325, #12509, #2753, #11925, #14604, #18680, #14964, #9495, #10862, #6847, #13084, #7659, #1206, #16251, #5501 ) ) ;
#18077=VERTEX_POINT ( 'NONE', #18148 ) ;
#18083=STYLED_ITEM ( 'NONE', ( #12536 ), #4884 ) ;
#18089=ORIENTED_EDGE ( 'NONE', *, *, #17907, .T. ) ;
#18121=VECTOR ( 'NONE', #10141, 1000.000000000000000 ) ;
#18128=CARTESIAN_POINT ( 'NONE',  ( 5.200000000000002842, 3.306546357697854226E-16, 2.700000000000000622 ) ) ;
#18148=CARTESIAN_POINT ( 'NONE',  ( 21.00000000000000355, 2.789133085058097101E-16, -2.055000000000000160 ) ) ;
#18156=CONICAL_SURFACE ( 'NONE', #529, 2.055000000000000160, 0.7853981633974639331 ) ;
#18158=EDGE_CURVE ( 'NONE', #16191, #1279, #12251, .T. ) ;
#18196=VECTOR ( 'NONE', #11447, 999.9999999999997726 ) ;
#18235=ORIENTED_EDGE ( 'NONE', *, *, #2143, .T. ) ;
#18241=CARTESIAN_POINT ( 'NONE',  ( 2.500000000000000000, 0.000000000000000000, 0.000000000000000000 ) ) ;
#18260=ORIENTED_EDGE ( 'NONE', *, *, #9715, .T. ) ;
#18277=DIRECTION ( 'NONE',  ( 0.000000000000000000, 0.000000000000000000, 1.000000000000000000 ) ) ;
#18287=LINE ( 'NONE', #18580, #3911 ) ;
#18315=DIRECTION ( 'NONE',  ( 0.000000000000000000, 0.000000000000000000, -1.000000000000000000 ) ) ;
#18332=ORIENTED_EDGE ( 'NONE', *, *, #17728, .F. ) ;
#18337=EDGE_CURVE ( 'NONE', #2698, #3664, #14517, .T. ) ;
#18341=VERTEX_POINT ( 'NONE', #16047 ) ;
#18349=DIRECTION ( 'NONE',  ( 0.000000000000000000, 0.000000000000000000, 1.000000000000000000 ) ) ;
#18357=DIRECTION ( 'NONE',  ( -0.000000000000000000, 1.287488025362403787E-15, 1.000000000000000000 ) ) ;
#18376=DIRECTION ( 'NONE',  ( 0.000000000000000000, 0.000000000000000000, 1.000000000000000000 ) ) ;
#18446=ORIENTED_EDGE ( 'NONE', *, *, #8262, .T. ) ;
#18483=DIRECTION ( 'NONE',  ( -1.000000000000000000, -0.000000000000000000, -0.000000000000000000 ) ) ;
#18487=CIRCLE ( 'NONE', #13929, 2.700000000000000622 ) ;
#18528=DIRECTION ( 'NONE',  ( -1.000000000000000000, -0.000000000000000000, -0.000000000000000000 ) ) ;
#18534=LINE ( 'NONE', #7182, #18121 ) ;
#18580=CARTESIAN_POINT ( 'NONE',  ( 2.500000000000000000, 2.357898499370431722, -2.818925648462311528E-15 ) ) ;
#18597=CARTESIAN_POINT ( 'NONE',  ( 2.500000000000000000, -2.357898499370432166, 3.035766082959412415E-15 ) ) ;
#18600=EDGE_LOOP ( 'NONE', ( #8297, #8935, #18651, #1224, #17939 ) ) ;
#18629=SURFACE_STYLE_FILL_AREA ( #13972 ) ;
#18640=CARTESIAN_POINT ( 'NONE',  ( 0.2500000000000002220, 0.000000000000000000, 0.000000000000000000 ) ) ;
#18651=ORIENTED_EDGE ( 'NONE', *, *, #9121, .F. ) ;
#18666=CARTESIAN_POINT ( 'NONE',  ( 21.00000000000000355, 0.000000000000000000, 0.000000000000000000 ) ) ;
#18680=ADVANCED_FACE ( 'NONE', ( #16798 ), #804, .T. ) ;
#18710=PRODUCT_DEFINITION_FORMATION_WITH_SPECIFIED_SOURCE ( 'ANY', '', #4043, .NOT_KNOWN. ) ;
#18715=VECTOR ( 'NONE', #12541, 1000.000000000000114 ) ;
#18730=PLANE ( 'NONE',  #2975 ) ;
#18732=CYLINDRICAL_SURFACE ( 'NONE', #5925, 2.500000000000000444 ) ;
#18752=ORIENTED_EDGE ( 'NONE', *, *, #8599, .F. ) ;
#18758=CARTESIAN_POINT ( 'NONE',  ( 2.500000000000000000, -1.178949249685214307, 2.042000000000001592 ) ) ;
#18766=CARTESIAN_POINT ( 'NONE',  ( 0.000000000000000000, 2.357898499370431722, -2.818925648462311528E-15 ) ) ;
#18786=AXIS2_PLACEMENT_3D ( 'NONE', #7739, #17751, #9265 ) ;
#18877=COLOUR_RGB('Black',0.12,0.14,0.17);
#18878=FILL_AREA_STYLE_COLOUR('',#18877);
#18879=FILL_AREA_STYLE('',(#18878));
#18880=SURFACE_STYLE_FILL_AREA(#18879);
#18881=SURFACE_SIDE_STYLE('',(#18880));
#18882=SURFACE_STYLE_USAGE(.BOTH.,#18881);
#18883=PRESENTATION_STYLE_ASSIGNMENT((#18882));
ENDSEC;
END-ISO-10303-21;
